ISO-10303-21;
HEADER;
FILE_DESCRIPTION (('STEP AP214'),
    '1' );
FILE_NAME ('hex bolt gradeab_iso_ISO 4014 - M12 x 120 x 30-N.step',
    '2026-10-18T20:16:25',
    ( '' ),
    ( '' ),
    'SwSTEP 2.0',
    'SolidWorks 2025',
    '' );
FILE_SCHEMA (( 'AUTOMOTIVE_DESIGN' ));
ENDSEC;

DATA;
#2=DIRECTION ( 'NONE',  ( 0.000000000000000000, 0.000000000000000000, -1.000000000000000000 ) ) ;
#24=CARTESIAN_POINT ( 'NONE',  ( 0.3552109633508558351, -3.484997970623677332, -9.000000000000000000 ) ) ;
#69=CARTESIAN_POINT ( 'NONE',  ( 6.899999999999999467, 5.196152422706624030, 9.000000000000001776 ) ) ;
#79=CARTESIAN_POINT ( 'NONE',  ( 0.000000000000000000, 0.000000000000000000, 9.000000000000000000 ) ) ;
#82=CARTESIAN_POINT ( 'NONE',  ( 6.900000000000000355, 0.000000000000000000, 0.000000000000000000 ) ) ;
#94=DIRECTION ( 'NONE',  ( 1.000000000000000000, 0.000000000000000000, 0.000000000000000000 ) ) ;
#99=ORIENTED_EDGE ( 'NONE', *, *, #3233, .T. ) ;
#152=CARTESIAN_POINT ( 'NONE',  ( 8.099999999999999645, 0.000000000000000000, 0.000000000000000000 ) ) ;
#173=DIRECTION ( 'NONE',  ( 0.000000000000000000, 0.000000000000000000, 1.000000000000000000 ) ) ;
#179=CIRCLE ( 'NONE', #30097, 0.5999999999999998668 ) ;
#223=CARTESIAN_POINT ( 'NONE',  ( 0.1482032042127262861, 2.204400401860216796, 9.000000000000001776 ) ) ;
#237=SHAPE_DEFINITION_REPRESENTATION ( #26098, #10307 ) ;
#263=DIRECTION ( 'NONE',  ( 0.000000000000000000, 0.000000000000000000, -1.000000000000000000 ) ) ;
#268=CARTESIAN_POINT ( 'NONE',  ( 0.000000000000000000, 1.102182119232617714E-15, -9.000000000000000000 ) ) ;
#281=VERTEX_POINT ( 'NONE', #19019 ) ;
#293=EDGE_CURVE ( 'NONE', #13653, #26600, #10904, .T. ) ;
#323=LINE ( 'NONE', #5317, #8177 ) ;
#360=AXIS2_PLACEMENT_3D ( 'NONE', #13665, #18184, #22851 ) ;
#427=ORIENTED_EDGE ( 'NONE', *, *, #26367, .F. ) ;
#447=CIRCLE ( 'NONE', #17897, 9.000000000000000000 ) ;
#462=CIRCLE ( 'NONE', #19386, 9.000000000000000000 ) ;
#474=FACE_OUTER_BOUND ( 'NONE', #14568, .T. ) ;
#508=CARTESIAN_POINT ( 'NONE',  ( 0.000000000000000000, 7.794228634059944483, -4.500000000000004441 ) ) ;
#511=CARTESIAN_POINT ( 'NONE',  ( 0.8038475772933696417, 10.39230484541327471, -1.336447385876663028E-16 ) ) ;
#589=ORIENTED_EDGE ( 'NONE', *, *, #10348, .F. ) ;
#614=ADVANCED_FACE ( 'NONE', ( #28465 ), #16596, .F. ) ;
#618=CARTESIAN_POINT ( 'NONE',  ( 0.000000000000000000, 0.000000000000000000, 0.000000000000000000 ) ) ;
#705=ORIENTED_EDGE ( 'NONE', *, *, #22488, .F. ) ;
#926=ORIENTED_EDGE ( 'NONE', *, *, #14035, .F. ) ;
#967=ORIENTED_EDGE ( 'NONE', *, *, #11204, .F. ) ;
#1029=EDGE_CURVE ( 'NONE', #14253, #23209, #26965, .T. ) ;
#1035=DIRECTION ( 'NONE',  ( -0.000000000000000000, 0.000000000000000000, -1.000000000000000000 ) ) ;
#1062=LINE ( 'NONE', #25066, #29718 ) ;
#1068=FACE_OUTER_BOUND ( 'NONE', #20155, .T. ) ;
#1096=CARTESIAN_POINT ( 'NONE',  ( 8.099999999999999645, 0.000000000000000000, 0.000000000000000000 ) ) ;
#1110=CARTESIAN_POINT ( 'NONE',  ( 6.899999999999999467, 10.39230484541327471, 0.000000000000000000 ) ) ;
#1112=EDGE_LOOP ( 'NONE', ( #7316, #18014, #2350, #6079, #17115, #6493 ) ) ;
#1131=AXIS2_PLACEMENT_3D ( 'NONE', #15422, #3582, #8431 ) ;
#1143=CARTESIAN_POINT ( 'NONE',  ( 6.899999999999999467, 9.000000000000000000, 0.000000000000000000 ) ) ;
#1155=AXIS2_PLACEMENT_3D ( 'NONE', #1770, #15808, #13644 ) ;
#1184=AXIS2_PLACEMENT_3D ( 'NONE', #30275, #2035, #11412 ) ;
#1250=CARTESIAN_POINT ( 'NONE',  ( 0.8038475772933646457, 5.196152422706634688, -9.000000000000001776 ) ) ;
#1262=EDGE_LOOP ( 'NONE', ( #5349, #15850, #2816 ) ) ;
#1286=VERTEX_POINT ( 'NONE', #28994 ) ;
#1328=ORIENTED_EDGE ( 'NONE', *, *, #17743, .T. ) ;
#1351=CONICAL_SURFACE ( 'NONE', #5825, 9.000000000000000000, 1.047197551196600296 ) ;
#1444=AXIS2_PLACEMENT_3D ( 'NONE', #23756, #17055, #24221 ) ;
#1446=AXIS2_PLACEMENT_3D ( 'NONE', #152, #26052, #4684 ) ;
#1481=CARTESIAN_POINT ( 'NONE',  ( 0.000000000000000000, -7.794228634059938265, -4.500000000000013323 ) ) ;
#1531=ORIENTED_EDGE ( 'NONE', *, *, #30532, .T. ) ;
#1709=ORIENTED_EDGE ( 'NONE', *, *, #11204, .T. ) ;
#1770=CARTESIAN_POINT ( 'NONE',  ( 6.900000000000000355, 0.000000000000000000, 0.000000000000000000 ) ) ;
#1776=B_SPLINE_CURVE_WITH_KNOTS ( 'NONE', 3,
 ( #25057, #10873, #5721, #3702, #19928, #29442 ),
 .UNSPECIFIED., .F., .F.,
 ( 4, 2, 4 ),
 ( 2.380730968220726544E-07, 0.002629065763328351790, 0.005257893453559881955 ),
 .UNSPECIFIED. ) ;
#1779=CARTESIAN_POINT ( 'NONE',  ( 7.500000000000000000, 5.196152422706634688, -9.000000000000001776 ) ) ;
#1785=AXIS2_PLACEMENT_3D ( 'NONE', #22998, #27857, #27696 ) ;
#1789=ADVANCED_FACE ( 'NONE', ( #7449 ), #14460, .T. ) ;
#1817=ORIENTED_EDGE ( 'NONE', *, *, #27673, .T. ) ;
#1846=AXIS2_PLACEMENT_3D ( 'NONE', #16145, #6484, #1954 ) ;
#1870=CARTESIAN_POINT ( 'NONE',  ( 0.8038475772933806329, -10.39230484541329247, 6.144194323733775069E-17 ) ) ;
#1898=ORIENTED_EDGE ( 'NONE', *, *, #24612, .T. ) ;
#1954=DIRECTION ( 'NONE',  ( 0.000000000000000000, 0.000000000000000000, 1.000000000000000000 ) ) ;
#2004=ORIENTED_EDGE ( 'NONE', *, *, #6342, .T. ) ;
#2014=EDGE_LOOP ( 'NONE', ( #18586, #30083, #10339 ) ) ;
#2020=LINE ( 'NONE', #12003, #27280 ) ;
#2026=EDGE_CURVE ( 'NONE', #18898, #12149, #21272, .T. ) ;
#2035=DIRECTION ( 'NONE',  ( 1.000000000000000000, 0.000000000000000000, 0.000000000000000000 ) ) ;
#2062=CARTESIAN_POINT ( 'NONE',  ( 7.500000000000000000, -5.196152422706639129, -9.000000000000000000 ) ) ;
#2065=ADVANCED_BREP_SHAPE_REPRESENTATION ( '', ( #23377, #7396 ), #3935 ) ;
#2121=FACE_OUTER_BOUND ( 'NONE', #29788, .T. ) ;
#2149=EDGE_CURVE ( 'NONE', #11604, #2369, #16151, .T. ) ;
#2170=EDGE_CURVE ( 'NONE', #18929, #12149, #21437, .T. ) ;
#2204=CARTESIAN_POINT ( 'NONE',  ( 0.000000000000000000, 0.000000000000000000, 9.000000000000000000 ) ) ;
#2210=CARTESIAN_POINT ( 'NONE',  ( 6.899999999999999467, 10.39230484541327471, 0.000000000000000000 ) ) ;
#2220=CARTESIAN_POINT ( 'NONE',  ( 0.01899995639453604460, 8.236198097127175544, 3.734486434573633495 ) ) ;
#2222=ORIENTED_EDGE ( 'NONE', *, *, #23631, .T. ) ;
#2250=PLANE ( 'NONE',  #26984 ) ;
#2318=CONICAL_SURFACE ( 'NONE', #8336, 9.000000000000000000, 1.047197551196600296 ) ;
#2330=ORIENTED_EDGE ( 'NONE', *, *, #28057, .F. ) ;
#2350=ORIENTED_EDGE ( 'NONE', *, *, #2149, .F. ) ;
#2359=CLOSED_SHELL ( 'NONE', ( #30752, #4651, #16613, #18838, #2702, #10709, #14144, #2545, #28819, #29250, #25498, #1789, #7141, #24614, #25569, #3111, #20463, #29219, #11132, #29966, #9178, #7035, #14131, #8068, #25389, #12788, #19144, #614, #13567 ) ) ;
#2365=AXIS2_PLACEMENT_3D ( 'NONE', #6048, #15398, #15710 ) ;
#2369=VERTEX_POINT ( 'NONE', #26273 ) ;
#2372=FACE_OUTER_BOUND ( 'NONE', #19598, .T. ) ;
#2384=ORIENTED_EDGE ( 'NONE', *, *, #13636, .F. ) ;
#2389=ORIENTED_EDGE ( 'NONE', *, *, #12052, .T. ) ;
#2402=CIRCLE ( 'NONE', #20333, 6.600000000000001421 ) ;
#2413=VERTEX_POINT ( 'NONE', #24395 ) ;
#2417=APPLICATION_CONTEXT ( 'automotive_design' ) ;
#2424=ORIENTED_EDGE ( 'NONE', *, *, #6315, .T. ) ;
#2469=AXIS2_PLACEMENT_3D ( 'NONE', #13908, #18596, #16544 ) ;
#2510=EDGE_CURVE ( 'NONE', #2413, #23760, #25104, .T. ) ;
#2545=ADVANCED_FACE ( 'NONE', ( #12053 ), #9702, .F. ) ;
#2603=DIRECTION ( 'NONE',  ( 0.000000000000000000, 0.000000000000000000, -1.000000000000000000 ) ) ;
#2609=DIRECTION ( 'NONE',  ( 1.000000000000000000, 0.000000000000000000, 0.000000000000000000 ) ) ;
#2621=VECTOR ( 'NONE', #4644, 1000.000000000000000 ) ;
#2660=VERTEX_POINT ( 'NONE', #19530 ) ;
#2673=CARTESIAN_POINT ( 'NONE',  ( 0.000000000000000000, -1.502314598737157848E-15, -9.000000000000001776 ) ) ;
#2702=ADVANCED_FACE ( 'NONE', ( #13295, #17657 ), #10167, .T. ) ;
#2741=ORIENTED_EDGE ( 'NONE', *, *, #12392, .F. ) ;
#2749=CARTESIAN_POINT ( 'NONE',  ( 6.632267977001171655E-15, -7.573738413550481496, 4.881900264494505315 ) ) ;
#2778=CARTESIAN_POINT ( 'NONE',  ( 0.000000000000000000, -1.502314598737157848E-15, -9.000000000000001776 ) ) ;
#2808=AXIS2_PLACEMENT_3D ( 'NONE', #12680, #24831, #10481 ) ;
#2816=ORIENTED_EDGE ( 'NONE', *, *, #20210, .T. ) ;
#2856=ORIENTED_EDGE ( 'NONE', *, *, #15096, .T. ) ;
#2947=CARTESIAN_POINT ( 'NONE',  ( 0.000000000000000000, 0.000000000000000000, 0.000000000000000000 ) ) ;
#3064=PLANE ( 'NONE',  #10811 ) ;
#3077=ORIENTED_EDGE ( 'NONE', *, *, #5666, .F. ) ;
#3094=ORIENTED_EDGE ( 'NONE', *, *, #13534, .F. ) ;
#3111=ADVANCED_FACE ( 'NONE', ( #9931 ), #3064, .F. ) ;
#3218=CARTESIAN_POINT ( 'NONE',  ( 126.5359999999999872, 0.000000000000000000, 0.000000000000000000 ) ) ;
#3233=EDGE_CURVE ( 'NONE', #16129, #1286, #28681, .T. ) ;
#3256=AXIS2_PLACEMENT_3D ( 'NONE', #24841, #22801, #10967 ) ;
#3345=CARTESIAN_POINT ( 'NONE',  ( 0.3563104543936100876, -6.049278984716131013, -7.522341449313008965 ) ) ;
#3378=PLANE ( 'NONE',  #6557 ) ;
#3483=DIRECTION ( 'NONE',  ( -1.000000000000000000, -0.000000000000000000, -0.000000000000000000 ) ) ;
#3514=CARTESIAN_POINT ( 'NONE',  ( 127.5000000000000000, 0.000000000000000000, 5.035999999999999588 ) ) ;
#3582=DIRECTION ( 'NONE',  ( -1.000000000000000000, -0.000000000000000000, -0.000000000000000000 ) ) ;
#3658=CARTESIAN_POINT ( 'NONE',  ( 0.8038475772931101826, -5.196152422707025487, -9.000000000000000000 ) ) ;
#3702=CARTESIAN_POINT ( 'NONE',  ( 0.07661102881317781443, 6.914460432017338398, 6.023803224821318913 ) ) ;
#3720=PLANE ( 'NONE',  #2365 ) ;
#3808=CARTESIAN_POINT ( 'NONE',  ( 6.899999999999999467, 10.39230484541327471, 0.000000000000000000 ) ) ;
#3880=VECTOR ( 'NONE', #20193, 1000.000000000000114 ) ;
#3898=EDGE_LOOP ( 'NONE', ( #13946, #30541, #21181, #4474, #3077, #19175 ) ) ;
#3917=ORIENTED_EDGE ( 'NONE', *, *, #6315, .F. ) ;
#3935=( GEOMETRIC_REPRESENTATION_CONTEXT ( 3 ) GLOBAL_UNCERTAINTY_ASSIGNED_CONTEXT ( ( #26681 ) ) GLOBAL_UNIT_ASSIGNED_CONTEXT ( ( #27417, #20529, #25375 ) ) REPRESENTATION_CONTEXT ( 'NONE', 'WORKASPACE' ) );
#3995=DIRECTION ( 'NONE',  ( 0.000000000000000000, 0.5000000000000006661, 0.8660254037844382635 ) ) ;
#4006=DIRECTION ( 'NONE',  ( 0.000000000000000000, 0.000000000000000000, -1.000000000000000000 ) ) ;
#4108=DIRECTION ( 'NONE',  ( -1.000000000000000000, -0.000000000000000000, -0.000000000000000000 ) ) ;
#4132=ORIENTED_EDGE ( 'NONE', *, *, #21013, .T. ) ;
#4145=LINE ( 'NONE', #27557, #6094 ) ;
#4214=VERTEX_POINT ( 'NONE', #6779 ) ;
#4267=ORIENTED_EDGE ( 'NONE', *, *, #23852, .F. ) ;
#4295=AXIS2_PLACEMENT_3D ( 'NONE', #7686, #7532, #7376 ) ;
#4364=B_SPLINE_CURVE_WITH_KNOTS ( 'NONE', 3,
 ( #18354, #10705, #13675, #18194, #30349, #17895 ),
 .UNSPECIFIED., .F., .F.,
 ( 4, 2, 4 ),
 ( 2.380730968221991799E-07, 0.002629065763328360898, 0.005257893453559900170 ),
 .UNSPECIFIED. ) ;
#4426=CARTESIAN_POINT ( 'NONE',  ( 127.5000000000000000, 0.000000000000000000, 0.000000000000000000 ) ) ;
#4474=ORIENTED_EDGE ( 'NONE', *, *, #12980, .F. ) ;
#4501=CARTESIAN_POINT ( 'NONE',  ( 8.099999999999999645, 0.000000000000000000, 0.000000000000000000 ) ) ;
#4553=ORIENTED_EDGE ( 'NONE', *, *, #9784, .T. ) ;
#4558=EDGE_CURVE ( 'NONE', #18898, #2369, #8951, .T. ) ;
#4644=DIRECTION ( 'NONE',  ( -1.000000000000000000, -0.000000000000000000, -0.000000000000000000 ) ) ;
#4651=ADVANCED_FACE ( 'NONE', ( #2372 ), #26076, .T. ) ;
#4684=DIRECTION ( 'NONE',  ( 0.000000000000000000, 0.000000000000000000, -1.000000000000000000 ) ) ;
#4740=DIRECTION ( 'NONE',  ( 0.000000000000000000, -0.8660254037844383745, 0.5000000000000006661 ) ) ;
#4857=CARTESIAN_POINT ( 'NONE',  ( 0.8038475772931101826, -5.196152422707025487, -9.000000000000000000 ) ) ;
#4918=CARTESIAN_POINT ( 'NONE',  ( 7.500000000000000000, 8.082668874372532992E-16, 6.600000000000001421 ) ) ;
#4930=DIRECTION ( 'NONE',  ( 1.000000000000000000, 0.000000000000000000, 0.000000000000000000 ) ) ;
#4981=CARTESIAN_POINT ( 'NONE',  ( 6.900000000000000355, -7.794228634059942706, 4.500000000000005329 ) ) ;
#5041=CARTESIAN_POINT ( 'NONE',  ( 7.500000000000000000, 5.196152422706634688, -9.000000000000001776 ) ) ;
#5134=EDGE_CURVE ( 'NONE', #7128, #10711, #17828, .T. ) ;
#5144=CARTESIAN_POINT ( 'NONE',  ( 0.1482032042127267857, 2.204400401860220793, -9.000000000000001776 ) ) ;
#5253=CARTESIAN_POINT ( 'NONE',  ( 7.500000000000000000, -10.39230484541329247, 8.776157072412030708E-17 ) ) ;
#5272=CIRCLE ( 'NONE', #16241, 6.000000000000001776 ) ;
#5274=DIRECTION ( 'NONE',  ( 0.000000000000000000, 0.000000000000000000, -1.000000000000000000 ) ) ;
#5280=ORIENTED_EDGE ( 'NONE', *, *, #2149, .T. ) ;
#5303=DIRECTION ( 'NONE',  ( 0.000000000000000000, 0.000000000000000000, -1.000000000000000000 ) ) ;
#5317=CARTESIAN_POINT ( 'NONE',  ( 6.899999999999999467, 5.196152422706624030, 9.000000000000001776 ) ) ;
#5325=ORIENTED_EDGE ( 'NONE', *, *, #6049, .T. ) ;
#5342=CARTESIAN_POINT ( 'NONE',  ( 127.5000000000000000, 0.000000000000000000, 0.000000000000000000 ) ) ;
#5349=ORIENTED_EDGE ( 'NONE', *, *, #12980, .T. ) ;
#5425=CARTESIAN_POINT ( 'NONE',  ( 6.899999999999999467, -5.196152422706639129, -9.000000000000000000 ) ) ;
#5437=CARTESIAN_POINT ( 'NONE',  ( 6.899999999999999467, 9.000000000000000000, 0.000000000000000000 ) ) ;
#5468=CIRCLE ( 'NONE', #30382, 5.035999999999999588 ) ;
#5515=ORIENTED_EDGE ( 'NONE', *, *, #2170, .F. ) ;
#5591=CIRCLE ( 'NONE', #26005, 6.000000000000001776 ) ;
#5666=EDGE_CURVE ( 'NONE', #2660, #18536, #23572, .T. ) ;
#5712=FACE_OUTER_BOUND ( 'NONE', #24372, .T. ) ;
#5721=CARTESIAN_POINT ( 'NONE',  ( 0.3563104543936347901, 6.049278984716042196, 7.522341449313135975 ) ) ;
#5754=DIRECTION ( 'NONE',  ( 1.000000000000000000, 0.000000000000000000, -0.000000000000000000 ) ) ;
#5768=EDGE_CURVE ( 'NONE', #16514, #281, #5591, .T. ) ;
#5825=AXIS2_PLACEMENT_3D ( 'NONE', #23624, #94, #9755 ) ;
#6048=CARTESIAN_POINT ( 'NONE',  ( 7.500000000000000000, 10.39230484541327471, 0.000000000000000000 ) ) ;
#6049=EDGE_CURVE ( 'NONE', #14664, #1286, #28818, .T. ) ;
#6079=ORIENTED_EDGE ( 'NONE', *, *, #18399, .F. ) ;
#6094=VECTOR ( 'NONE', #29902, 1000.000000000000000 ) ;
#6111=CARTESIAN_POINT ( 'NONE',  ( 7.500000000000000000, 0.000000000000000000, 0.000000000000000000 ) ) ;
#6296=EDGE_CURVE ( 'NONE', #23760, #14253, #4364, .T. ) ;
#6315=EDGE_CURVE ( 'NONE', #7923, #10711, #13524, .T. ) ;
#6327=DIRECTION ( 'NONE',  ( 0.000000000000000000, 0.8660254037844382635, -0.5000000000000006661 ) ) ;
#6337=ORIENTED_EDGE ( 'NONE', *, *, #12052, .F. ) ;
#6342=EDGE_CURVE ( 'NONE', #7128, #281, #4145, .T. ) ;
#6453=CARTESIAN_POINT ( 'NONE',  ( 0.000000000000000000, 0.000000000000000000, 0.000000000000000000 ) ) ;
#6459=CARTESIAN_POINT ( 'NONE',  ( 0.5590800469813657081, 9.968355046870088998, 0.7343025909353930736 ) ) ;
#6460=CIRCLE ( 'NONE', #2469, 9.000000000000000000 ) ;
#6473=EDGE_CURVE ( 'NONE', #4214, #16129, #20054, .T. ) ;
#6484=DIRECTION ( 'NONE',  ( -1.000000000000000000, -0.000000000000000000, -0.000000000000000000 ) ) ;
#6493=ORIENTED_EDGE ( 'NONE', *, *, #26799, .F. ) ;
#6509=DIRECTION ( 'NONE',  ( 0.000000000000000000, 0.5000000000000015543, -0.8660254037844378194 ) ) ;
#6554=CARTESIAN_POINT ( 'NONE',  ( 0.1469846612282587339, -8.891930899535442023, -2.598723904613021496 ) ) ;
#6557=AXIS2_PLACEMENT_3D ( 'NONE', #27701, #6327, #3995 ) ;
#6691=LINE ( 'NONE', #16203, #30842 ) ;
#6716=EDGE_CURVE ( 'NONE', #27888, #4214, #27831, .T. ) ;
#6728=EDGE_CURVE ( 'NONE', #7440, #11068, #15597, .T. ) ;
#6779=CARTESIAN_POINT ( 'NONE',  ( 6.900000000000000355, 7.794228634059940042, 4.500000000000011546 ) ) ;
#6871=AXIS2_PLACEMENT_3D ( 'NONE', #4501, #30537, #11669 ) ;
#7007=CARTESIAN_POINT ( 'NONE',  ( 0.000000000000000000, -7.794228634059938265, -4.500000000000013323 ) ) ;
#7035=ADVANCED_FACE ( 'NONE', ( #10637 ), #30553, .T. ) ;
#7128=VERTEX_POINT ( 'NONE', #13895 ) ;
#7131=PLANE ( 'NONE',  #28789 ) ;
#7141=ADVANCED_FACE ( 'NONE', ( #20742 ), #11705, .T. ) ;
#7164=CARTESIAN_POINT ( 'NONE',  ( 0.09252763182292866873, -8.674330214978059672, -2.975619346028175904 ) ) ;
#7206=CARTESIAN_POINT ( 'NONE',  ( 8.099999999999999645, 0.000000000000000000, 0.000000000000000000 ) ) ;
#7293=AXIS2_PLACEMENT_3D ( 'NONE', #29152, #7785, #17298 ) ;
#7316=ORIENTED_EDGE ( 'NONE', *, *, #2026, .F. ) ;
#7371=ORIENTED_EDGE ( 'NONE', *, *, #23631, .F. ) ;
#7376=DIRECTION ( 'NONE',  ( -0.000000000000000000, 0.000000000000000000, 1.000000000000000000 ) ) ;
#7396=AXIS2_PLACEMENT_3D ( 'NONE', #9486, #28514, #21014 ) ;
#7400=AXIS2_PLACEMENT_3D ( 'NONE', #23962, #2609, #263 ) ;
#7440=VERTEX_POINT ( 'NONE', #25251 ) ;
#7449=FACE_OUTER_BOUND ( 'NONE', #18607, .T. ) ;
#7514=EDGE_CURVE ( 'NONE', #10711, #7128, #24521, .T. ) ;
#7532=DIRECTION ( 'NONE',  ( -1.000000000000000000, 0.000000000000000000, -0.000000000000000000 ) ) ;
#7565=CARTESIAN_POINT ( 'NONE',  ( 0.01885174614965954773, 0.8831628876357842106, 9.000000000000003553 ) ) ;
#7592=CARTESIAN_POINT ( 'NONE',  ( 6.899999999999999467, 9.000000000000000000, 0.000000000000000000 ) ) ;
#7638=VERTEX_POINT ( 'NONE', #4918 ) ;
#7659=CARTESIAN_POINT ( 'NONE',  ( 6.900000000000000355, 0.000000000000000000, 9.000000000000000000 ) ) ;
#7686=CARTESIAN_POINT ( 'NONE',  ( 127.5000000000000000, 0.000000000000000000, 0.000000000000000000 ) ) ;
#7709=DIRECTION ( 'NONE',  ( 1.000000000000000000, 0.000000000000000000, -0.000000000000000000 ) ) ;
#7726=ORIENTED_EDGE ( 'NONE', *, *, #27673, .F. ) ;
#7770=CONICAL_SURFACE ( 'NONE', #15224, 9.000000000000000000, 1.047197551196600296 ) ;
#7771=DIRECTION ( 'NONE',  ( 1.000000000000000000, 0.000000000000000000, -0.000000000000000000 ) ) ;
#7785=DIRECTION ( 'NONE',  ( 0.000000000000000000, -1.000000000000000000, 0.000000000000000000 ) ) ;
#7859=AXIS2_PLACEMENT_3D ( 'NONE', #29998, #27966, #15637 ) ;
#7923=VERTEX_POINT ( 'NONE', #3514 ) ;
#7932=DIRECTION ( 'NONE',  ( 0.000000000000000000, 0.000000000000000000, -1.000000000000000000 ) ) ;
#7986=CARTESIAN_POINT ( 'NONE',  ( 0.000000000000000000, 0.000000000000000000, 6.000000000000001776 ) ) ;
#7999=LINE ( 'NONE', #12828, #24717 ) ;
#8032=AXIS2_PLACEMENT_3D ( 'NONE', #19695, #7709, #15323 ) ;
#8068=ADVANCED_FACE ( 'NONE', ( #19216 ), #26240, .F. ) ;
#8086=DIRECTION ( 'NONE',  ( 1.000000000000000000, 0.000000000000000000, 0.000000000000000000 ) ) ;
#8177=VECTOR ( 'NONE', #22002, 1000.000000000000000 ) ;
#8304=DIRECTION ( 'NONE',  ( 0.000000000000000000, 0.000000000000000000, -1.000000000000000000 ) ) ;
#8336=AXIS2_PLACEMENT_3D ( 'NONE', #20593, #30118, #23394 ) ;
#8431=DIRECTION ( 'NONE',  ( 0.000000000000000000, 0.000000000000000000, 1.000000000000000000 ) ) ;
#8481=AXIS2_PLACEMENT_3D ( 'NONE', #26443, #9904, #19419 ) ;
#8547=CARTESIAN_POINT ( 'NONE',  ( 7.500000000000000000, 0.000000000000000000, 0.000000000000000000 ) ) ;
#8677=CYLINDRICAL_SURFACE ( 'NONE', #26234, 6.000000000000001776 ) ;
#8756=ORIENTED_EDGE ( 'NONE', *, *, #6473, .F. ) ;
#8769=DIRECTION ( 'NONE',  ( 0.000000000000000000, 0.000000000000000000, 1.000000000000000000 ) ) ;
#8783=CARTESIAN_POINT ( 'NONE',  ( 0.5584673446549298648, -9.967293815311123240, 0.7361406979141417173 ) ) ;
#8787=DIRECTION ( 'NONE',  ( 0.000000000000000000, -0.5000000000000012212, 0.8660254037844380415 ) ) ;
#8849=VECTOR ( 'NONE', #12514, 999.9999999999998863 ) ;
#8951=LINE ( 'NONE', #21694, #21743 ) ;
#8973=DIRECTION ( 'NONE',  ( 0.000000000000000000, 1.000000000000000000, -1.669238443041286689E-16 ) ) ;
#9017=EDGE_CURVE ( 'NONE', #26600, #14545, #12571, .T. ) ;
#9132=ORIENTED_EDGE ( 'NONE', *, *, #26718, .T. ) ;
#9178=ADVANCED_FACE ( 'NONE', ( #25450 ), #2318, .T. ) ;
#9284=EDGE_LOOP ( 'NONE', ( #18288, #22447, #27001 ) ) ;
#9486=CARTESIAN_POINT ( 'NONE',  ( 0.000000000000000000, 0.000000000000000000, 0.000000000000000000 ) ) ;
#9505=ORIENTED_EDGE ( 'NONE', *, *, #2510, .T. ) ;
#9519=CARTESIAN_POINT ( 'NONE',  ( 0.5612050131688016696, 4.355613924421565919, -9.000000000000003553 ) ) ;
#9593=DIRECTION ( 'NONE',  ( -1.000000000000000000, -0.000000000000000000, -0.000000000000000000 ) ) ;
#9609=EDGE_CURVE ( 'NONE', #15949, #14253, #15799, .T. ) ;
#9696=DIRECTION ( 'NONE',  ( -1.000000000000000000, -0.000000000000000000, -0.000000000000000000 ) ) ;
#9702=PLANE ( 'NONE',  #4295 ) ;
#9737=EDGE_CURVE ( 'NONE', #18512, #16129, #10689, .T. ) ;
#9755=DIRECTION ( 'NONE',  ( 0.000000000000000000, 0.000000000000000000, -1.000000000000000000 ) ) ;
#9778=ORIENTED_EDGE ( 'NONE', *, *, #5768, .F. ) ;
#9784=EDGE_CURVE ( 'NONE', #1286, #18512, #30473, .T. ) ;
#9833=DIRECTION ( 'NONE',  ( 1.000000000000000000, 0.000000000000000000, 0.000000000000000000 ) ) ;
#9854=CARTESIAN_POINT ( 'NONE',  ( 0.09252763182292195188, 6.914127053141852386, -6.024380653971844524 ) ) ;
#9904=DIRECTION ( 'NONE',  ( 0.000000000000000000, 0.000000000000000000, -1.000000000000000000 ) ) ;
#9931=FACE_OUTER_BOUND ( 'NONE', #10255, .T. ) ;
#10017=DIRECTION ( 'NONE',  ( -1.000000000000000000, -0.000000000000000000, -0.000000000000000000 ) ) ;
#10072=EDGE_LOOP ( 'NONE', ( #5280, #23065, #30610 ) ) ;
#10095=AXIS2_PLACEMENT_3D ( 'NONE', #28745, #11915, #23583 ) ;
#10108=EDGE_CURVE ( 'NONE', #12149, #4214, #25217, .T. ) ;
#10118=VECTOR ( 'NONE', #8787, 999.9999999999998863 ) ;
#10167=PLANE ( 'NONE',  #2808 ) ;
#10174=FACE_OUTER_BOUND ( 'NONE', #12818, .T. ) ;
#10244=DIRECTION ( 'NONE',  ( 1.000000000000000000, 0.000000000000000000, -0.000000000000000000 ) ) ;
#10255=EDGE_LOOP ( 'NONE', ( #30776, #427, #10416, #6337, #25171, #18383 ) ) ;
#10307=SHAPE_REPRESENTATION ( 'hex bolt gradeab_iso_ISO 4014 - M12 x 120 x 30-N', ( #7396 ), #3935 ) ;
#10339=ORIENTED_EDGE ( 'NONE', *, *, #10108, .T. ) ;
#10348=EDGE_CURVE ( 'NONE', #26161, #26600, #28808, .T. ) ;
#10416=ORIENTED_EDGE ( 'NONE', *, *, #24566, .F. ) ;
#10481=DIRECTION ( 'NONE',  ( -0.000000000000000000, 0.000000000000000000, -1.000000000000000000 ) ) ;
#10533=CARTESIAN_POINT ( 'NONE',  ( 0.09252763182293005650, -6.914127053141865709, 6.024380653971853405 ) ) ;
#10574=APPLICATION_CONTEXT ( 'automotive_design' ) ;
#10589=EDGE_CURVE ( 'NONE', #1286, #7440, #15273, .T. ) ;
#10632=DIRECTION ( 'NONE',  ( -0.7071067811865541231, 8.659560562354850274E-17, -0.7071067811865408004 ) ) ;
#10637=FACE_OUTER_BOUND ( 'NONE', #1262, .T. ) ;
#10689=LINE ( 'NONE', #22535, #3880 ) ;
#10705=CARTESIAN_POINT ( 'NONE',  ( 0.5584673446549203168, 9.967293815311105476, -0.7361406979141401630 ) ) ;
#10709=ADVANCED_FACE ( 'NONE', ( #20514 ), #8677, .T. ) ;
#10711=VERTEX_POINT ( 'NONE', #26546 ) ;
#10722=VERTEX_POINT ( 'NONE', #28731 ) ;
#10792=CARTESIAN_POINT ( 'NONE',  ( 0.000000000000000000, 0.000000000000000000, 0.000000000000000000 ) ) ;
#10807=CYLINDRICAL_SURFACE ( 'NONE', #15003, 9.000000000000000000 ) ;
#10811=AXIS2_PLACEMENT_3D ( 'NONE', #20199, #27400, #1035 ) ;
#10818=FACE_OUTER_BOUND ( 'NONE', #18560, .T. ) ;
#10873=CARTESIAN_POINT ( 'NONE',  ( 0.5584673446549135445, 5.621163452808791483, 8.263859302085863945 ) ) ;
#10904=B_SPLINE_CURVE_WITH_KNOTS ( 'NONE', 3,
 ( #7007, #28530, #14325, #7164, #6554, #23217, #16066, #1870 ),
 .UNSPECIFIED., .F., .F.,
 ( 4, 2, 2, 4 ),
 ( 0.005257893453559869812, 0.006567392922673212161, 0.007876892391786554509, 0.01049589133001323921 ),
 .UNSPECIFIED. ) ;
#10915=DIRECTION ( 'NONE',  ( 0.000000000000000000, 0.000000000000000000, -1.000000000000000000 ) ) ;
#10967=DIRECTION ( 'NONE',  ( 0.000000000000000000, 0.000000000000000000, 1.000000000000000000 ) ) ;
#10997=ORIENTED_EDGE ( 'NONE', *, *, #18399, .T. ) ;
#11068=VERTEX_POINT ( 'NONE', #4981 ) ;
#11132=ADVANCED_FACE ( 'NONE', ( #474 ), #7770, .T. ) ;
#11171=DIRECTION ( 'NONE',  ( 0.000000000000000000, -1.000000000000000000, 0.000000000000000000 ) ) ;
#11181=ORIENTED_EDGE ( 'NONE', *, *, #3233, .F. ) ;
#11204=EDGE_CURVE ( 'NONE', #281, #16514, #5272, .T. ) ;
#11251=EDGE_LOOP ( 'NONE', ( #22935, #2384, #18490, #24578, #13485, #11601 ) ) ;
#11273=DIRECTION ( 'NONE',  ( 0.000000000000000000, -0.5000000000000006661, -0.8660254037844382635 ) ) ;
#11287=CARTESIAN_POINT ( 'NONE',  ( 0.8038475772933696417, 10.39230484541327471, -1.336447385876663028E-16 ) ) ;
#11307=ORIENTED_EDGE ( 'NONE', *, *, #30007, .F. ) ;
#11386=CARTESIAN_POINT ( 'NONE',  ( 6.899999999999999467, 5.196152422706634688, -9.000000000000001776 ) ) ;
#11412=DIRECTION ( 'NONE',  ( 0.000000000000000000, 0.000000000000000000, -1.000000000000000000 ) ) ;
#11414=CIRCLE ( 'NONE', #23353, 9.000000000000000000 ) ;
#11484=DIRECTION ( 'NONE',  ( 0.000000000000000000, 0.000000000000000000, 1.000000000000000000 ) ) ;
#11545=EDGE_CURVE ( 'NONE', #26314, #29153, #1062, .T. ) ;
#11601=ORIENTED_EDGE ( 'NONE', *, *, #10589, .F. ) ;
#11604=VERTEX_POINT ( 'NONE', #30616 ) ;
#11640=CARTESIAN_POINT ( 'NONE',  ( 0.000000000000000000, 0.000000000000000000, 0.000000000000000000 ) ) ;
#11669=DIRECTION ( 'NONE',  ( 0.000000000000000000, 0.000000000000000000, -1.000000000000000000 ) ) ;
#11705=PLANE ( 'NONE',  #1184 ) ;
#11822=ORIENTED_EDGE ( 'NONE', *, *, #11545, .T. ) ;
#11864=CARTESIAN_POINT ( 'NONE',  ( 7.500000000000000000, 0.000000000000000000, 0.000000000000000000 ) ) ;
#11915=DIRECTION ( 'NONE',  ( -0.000000000000000000, 0.8660254037844378194, 0.5000000000000015543 ) ) ;
#11927=ORIENTED_EDGE ( 'NONE', *, *, #6716, .F. ) ;
#11955=ORIENTED_EDGE ( 'NONE', *, *, #9737, .T. ) ;
#12003=CARTESIAN_POINT ( 'NONE',  ( 6.899999999999999467, -10.39230484541329247, 8.776157072412030708E-17 ) ) ;
#12013=ORIENTED_EDGE ( 'NONE', *, *, #12392, .T. ) ;
#12047=DIRECTION ( 'NONE',  ( 0.000000000000000000, 0.000000000000000000, 1.000000000000000000 ) ) ;
#12052=EDGE_CURVE ( 'NONE', #11604, #14545, #6460, .T. ) ;
#12053=FACE_OUTER_BOUND ( 'NONE', #25390, .T. ) ;
#12069=VECTOR ( 'NONE', #4108, 1000.000000000000000 ) ;
#12071=ORIENTED_EDGE ( 'NONE', *, *, #23082, .F. ) ;
#12149=VERTEX_POINT ( 'NONE', #7659 ) ;
#12186=DIRECTION ( 'NONE',  ( -1.000000000000000000, -0.000000000000000000, -0.000000000000000000 ) ) ;
#12188=CARTESIAN_POINT ( 'NONE',  ( 0.5595136366802740957, -4.349754824395941633, -9.000000000000000000 ) ) ;
#12237=CARTESIAN_POINT ( 'NONE',  ( 0.000000000000000000, 0.000000000000000000, 9.000000000000000000 ) ) ;
#12240=ORIENTED_EDGE ( 'NONE', *, *, #19068, .T. ) ;
#12259=CARTESIAN_POINT ( 'NONE',  ( 0.8038475772933700858, -5.196152422706651564, 9.000000000000001776 ) ) ;
#12332=CARTESIAN_POINT ( 'NONE',  ( 4.950437002841800198E-16, 0.4400770685579611374, -9.000000000000005329 ) ) ;
#12392=EDGE_CURVE ( 'NONE', #27888, #23760, #6691, .T. ) ;
#12442=DIRECTION ( 'NONE',  ( 0.000000000000000000, 0.000000000000000000, 1.000000000000000000 ) ) ;
#12450=EDGE_LOOP ( 'NONE', ( #9778, #19065, #4267, #16734 ) ) ;
#12456=B_SPLINE_CURVE_WITH_KNOTS ( 'NONE', 3,
 ( #23558, #26217, #18744, #21213, #30743, #2204 ),
 .UNSPECIFIED., .F., .F.,
 ( 4, 2, 4 ),
 ( 0.009719890944573148991, 0.01235036185894307706, 0.01498083277331300339 ),
 .UNSPECIFIED. ) ;
#12465=PLANE ( 'NONE',  #14475 ) ;
#12469=AXIS2_PLACEMENT_3D ( 'NONE', #6111, #29522, #15626 ) ;
#12514=DIRECTION ( 'NONE',  ( 0.000000000000000000, -0.5000000000000012212, 0.8660254037844380415 ) ) ;
#12571=B_SPLINE_CURVE_WITH_KNOTS ( 'NONE', 3,
 ( #27664, #8783, #27973, #18614, #18309, #30454 ),
 .UNSPECIFIED., .F., .F.,
 ( 4, 2, 4 ),
 ( 2.380730968223702541E-07, 0.002629065763328367403, 0.005257893453559912313 ),
 .UNSPECIFIED. ) ;
#12576=CARTESIAN_POINT ( 'NONE',  ( 0.01899995639454664029, -7.352259170992735626, 5.265513565426390485 ) ) ;
#12662=CARTESIAN_POINT ( 'NONE',  ( 0.8038475772931101826, -5.196152422707025487, -9.000000000000000000 ) ) ;
#12680=CARTESIAN_POINT ( 'NONE',  ( 7.500000000000000000, 4.336808689942017736E-15, -17.99999999999998224 ) ) ;
#12687=FACE_OUTER_BOUND ( 'NONE', #24807, .T. ) ;
#12703=DIRECTION ( 'NONE',  ( 1.000000000000000000, 0.000000000000000000, 0.000000000000000000 ) ) ;
#12788=ADVANCED_FACE ( 'NONE', ( #16925 ), #17228, .F. ) ;
#12818=EDGE_LOOP ( 'NONE', ( #16540, #15117, #19184, #12071, #926, #27568 ) ) ;
#12828=CARTESIAN_POINT ( 'NONE',  ( 127.5000000000000000, 6.167321280506070407E-16, -5.035999999999999588 ) ) ;
#12919=FACE_OUTER_BOUND ( 'NONE', #26885, .T. ) ;
#12980=EDGE_CURVE ( 'NONE', #18536, #13653, #29125, .T. ) ;
#12999=CARTESIAN_POINT ( 'NONE',  ( 6.899999999999999467, 9.000000000000000000, 0.000000000000000000 ) ) ;
#13063=EDGE_CURVE ( 'NONE', #11604, #2413, #462, .T. ) ;
#13295=FACE_BOUND ( 'NONE', #24371, .T. ) ;
#13300=EDGE_LOOP ( 'NONE', ( #2222, #18376, #15849, #3917 ) ) ;
#13353=AXIS2_PLACEMENT_3D ( 'NONE', #3218, #24275, #12442 ) ;
#13460=DIRECTION ( 'NONE',  ( 1.000000000000000000, 0.000000000000000000, 0.000000000000000000 ) ) ;
#13485=ORIENTED_EDGE ( 'NONE', *, *, #6728, .F. ) ;
#13489=CARTESIAN_POINT ( 'NONE',  ( 0.3570196857253507550, 9.540868182094909500, 1.474731560294324284 ) ) ;
#13524=LINE ( 'NONE', #29731, #27038 ) ;
#13534=EDGE_CURVE ( 'NONE', #14664, #18929, #11414, .T. ) ;
#13567=ADVANCED_FACE ( 'NONE', ( #12919 ), #14870, .F. ) ;
#13636=EDGE_CURVE ( 'NONE', #18929, #14664, #447, .T. ) ;
#13644=DIRECTION ( 'NONE',  ( 0.000000000000000000, 0.000000000000000000, 1.000000000000000000 ) ) ;
#13653=VERTEX_POINT ( 'NONE', #23014 ) ;
#13655=AXIS2_PLACEMENT_3D ( 'NONE', #26110, #4740, #21430 ) ;
#13665=CARTESIAN_POINT ( 'NONE',  ( 0.000000000000000000, 0.000000000000000000, 0.000000000000000000 ) ) ;
#13668=B_SPLINE_CURVE_WITH_KNOTS ( 'NONE', 3,
 ( #16694, #9519, #28402, #5144, #19037, #21831, #12332, #24004 ),
 .UNSPECIFIED., .F., .F.,
 ( 4, 2, 2, 4 ),
 ( 0.02518894967656377937, 0.02782118485464665780, 0.02913730244368809702, 0.03045342003272953624 ),
 .UNSPECIFIED. ) ;
#13675=CARTESIAN_POINT ( 'NONE',  ( 0.3563104543936387314, 9.539178283403856540, -1.477658550686871575 ) ) ;
#13864=ORIENTED_EDGE ( 'NONE', *, *, #9017, .F. ) ;
#13895=CARTESIAN_POINT ( 'NONE',  ( 126.5359999999999872, 7.347880794884121708E-16, -6.000000000000001776 ) ) ;
#13908=CARTESIAN_POINT ( 'NONE',  ( 0.000000000000000000, 0.000000000000000000, 0.000000000000000000 ) ) ;
#13946=ORIENTED_EDGE ( 'NONE', *, *, #15096, .F. ) ;
#14035=EDGE_CURVE ( 'NONE', #18512, #23209, #27839, .T. ) ;
#14131=ADVANCED_FACE ( 'NONE', ( #10174 ), #26242, .F. ) ;
#14144=ADVANCED_FACE ( 'NONE', ( #12687 ), #23144, .T. ) ;
#14253=VERTEX_POINT ( 'NONE', #508 ) ;
#14298=FACE_OUTER_BOUND ( 'NONE', #12450, .T. ) ;
#14325=CARTESIAN_POINT ( 'NONE',  ( 0.01899995639454398616, -8.236198097127184425, -3.734486434573641933 ) ) ;
#14376=PRODUCT_DEFINITION_FORMATION_WITH_SPECIFIED_SOURCE ( 'ANY', '', #23856, .NOT_KNOWN. ) ;
#14417=EDGE_LOOP ( 'NONE', ( #29938, #2004, #1709, #30335 ) ) ;
#14460=PLANE ( 'NONE',  #7400 ) ;
#14475=AXIS2_PLACEMENT_3D ( 'NONE', #5437, #8086, #21953 ) ;
#14517=ORIENTED_EDGE ( 'NONE', *, *, #9737, .F. ) ;
#14538=DIRECTION ( 'NONE',  ( 0.000000000000000000, 0.000000000000000000, -1.000000000000000000 ) ) ;
#14545=VERTEX_POINT ( 'NONE', #30858 ) ;
#14552=DIRECTION ( 'NONE',  ( 0.000000000000000000, 0.000000000000000000, 1.000000000000000000 ) ) ;
#14568=EDGE_LOOP ( 'NONE', ( #10997, #2389, #20224 ) ) ;
#14581=CARTESIAN_POINT ( 'NONE',  ( 0.8038475772933620922, 5.196152422706624030, 9.000000000000001776 ) ) ;
#14598=ORIENTED_EDGE ( 'NONE', *, *, #21059, .F. ) ;
#14607=DIRECTION ( 'NONE',  ( 1.000000000000000000, 0.000000000000000000, 0.000000000000000000 ) ) ;
#14664=VERTEX_POINT ( 'NONE', #29478 ) ;
#14700=ORIENTED_EDGE ( 'NONE', *, *, #21059, .T. ) ;
#14752=DIRECTION ( 'NONE',  ( -1.000000000000000000, -0.000000000000000000, -0.000000000000000000 ) ) ;
#14841=TOROIDAL_SURFACE ( 'NONE', #6871, 6.600000000000001421, 0.5999999999999999778 ) ;
#14853=DIRECTION ( 'NONE',  ( -1.000000000000000000, -0.000000000000000000, -0.000000000000000000 ) ) ;
#14855=ORIENTED_EDGE ( 'NONE', *, *, #6296, .F. ) ;
#14870=TOROIDAL_SURFACE ( 'NONE', #1446, 6.600000000000001421, 0.5999999999999999778 ) ;
#14909=CARTESIAN_POINT ( 'NONE',  ( 6.899999999999999467, -10.39230484541329247, 0.000000000000000000 ) ) ;
#14946=EDGE_CURVE ( 'NONE', #16514, #7638, #179, .T. ) ;
#15003=AXIS2_PLACEMENT_3D ( 'NONE', #20322, #3483, #27812 ) ;
#15004=DIRECTION ( 'NONE',  ( -0.000000000000000000, 1.669238443041286689E-16, 1.000000000000000000 ) ) ;
#15069=ORIENTED_EDGE ( 'NONE', *, *, #24566, .T. ) ;
#15096=EDGE_CURVE ( 'NONE', #26161, #7440, #16958, .T. ) ;
#15117=ORIENTED_EDGE ( 'NONE', *, *, #5666, .T. ) ;
#15159=EDGE_LOOP ( 'NONE', ( #14517, #28826, #15875, #14855, #2741, #14598 ) ) ;
#15191=CARTESIAN_POINT ( 'NONE',  ( 0.3570196857253563061, -6.047589086025013216, 7.525268439705684820 ) ) ;
#15224=AXIS2_PLACEMENT_3D ( 'NONE', #618, #9833, #5303 ) ;
#15273=CIRCLE ( 'NONE', #1846, 9.000000000000000000 ) ;
#15287=CARTESIAN_POINT ( 'NONE',  ( 0.000000000000000000, 7.794228634059944483, -4.500000000000004441 ) ) ;
#15321=AXIS2_PLACEMENT_3D ( 'NONE', #27962, #18140, #8769 ) ;
#15323=DIRECTION ( 'NONE',  ( 0.000000000000000000, 0.000000000000000000, -1.000000000000000000 ) ) ;
#15345=CARTESIAN_POINT ( 'NONE',  ( 3.808260130855334324E-15, -7.351593252548093815, -5.266666970006190773 ) ) ;
#15378=VECTOR ( 'NONE', #9593, 1000.000000000000000 ) ;
#15398=DIRECTION ( 'NONE',  ( 0.000000000000000000, -0.8660254037844380415, -0.5000000000000012212 ) ) ;
#15422=CARTESIAN_POINT ( 'NONE',  ( 126.5359999999999872, 0.000000000000000000, 0.000000000000000000 ) ) ;
#15448=ORIENTED_EDGE ( 'NONE', *, *, #14946, .F. ) ;
#15597=CIRCLE ( 'NONE', #1155, 9.000000000000000000 ) ;
#15626=DIRECTION ( 'NONE',  ( 0.000000000000000000, 0.000000000000000000, -1.000000000000000000 ) ) ;
#15637=DIRECTION ( 'NONE',  ( 0.000000000000000000, 0.000000000000000000, 1.000000000000000000 ) ) ;
#15710=DIRECTION ( 'NONE',  ( 0.000000000000000000, 0.5000000000000012212, -0.8660254037844380415 ) ) ;
#15799=CIRCLE ( 'NONE', #23752, 9.000000000000000000 ) ;
#15808=DIRECTION ( 'NONE',  ( -1.000000000000000000, -0.000000000000000000, -0.000000000000000000 ) ) ;
#15811=CARTESIAN_POINT ( 'NONE',  ( 0.5584673446548731324, -5.621163452808898953, -8.263859302085702296 ) ) ;
#15818=AXIS2_PLACEMENT_3D ( 'NONE', #18555, #18860, #16201 ) ;
#15849=ORIENTED_EDGE ( 'NONE', *, *, #7514, .F. ) ;
#15850=ORIENTED_EDGE ( 'NONE', *, *, #26367, .T. ) ;
#15875=ORIENTED_EDGE ( 'NONE', *, *, #1029, .F. ) ;
#15877=EDGE_CURVE ( 'NONE', #2660, #1286, #16357, .T. ) ;
#15949=VERTEX_POINT ( 'NONE', #2778 ) ;
#16066=CARTESIAN_POINT ( 'NONE',  ( 0.5590800469813748119, -9.968355046870097880, -0.7343025909353961822 ) ) ;
#16129=VERTEX_POINT ( 'NONE', #26921 ) ;
#16145=CARTESIAN_POINT ( 'NONE',  ( 6.900000000000000355, 0.000000000000000000, 0.000000000000000000 ) ) ;
#16151=B_SPLINE_CURVE_WITH_KNOTS ( 'NONE', 3,
 ( #12237, #21590, #7565, #19989, #223, #28931, #21738, #14581 ),
 .UNSPECIFIED., .F., .F.,
 ( 4, 2, 2, 4 ),
 ( 0.01498083277331300339, 0.01629713195395227077, 0.01761343113459154161, 0.02024602949587007983 ),
 .UNSPECIFIED. ) ;
#16201=DIRECTION ( 'NONE',  ( 0.000000000000000000, 0.000000000000000000, 1.000000000000000000 ) ) ;
#16203=CARTESIAN_POINT ( 'NONE',  ( 7.500000000000000000, 10.39230484541327471, 0.000000000000000000 ) ) ;
#16241=AXIS2_PLACEMENT_3D ( 'NONE', #1096, #22141, #24635 ) ;
#16251=LINE ( 'NONE', #27967, #18594 ) ;
#16269=CARTESIAN_POINT ( 'NONE',  ( 0.000000000000000000, 0.000000000000000000, 0.000000000000000000 ) ) ;
#16357=LINE ( 'NONE', #16962, #27116 ) ;
#16364=DIRECTION ( 'NONE',  ( -1.000000000000000000, -0.000000000000000000, -0.000000000000000000 ) ) ;
#16403=CARTESIAN_POINT ( 'NONE',  ( 127.5000000000000000, 6.757601037695096551E-16, -5.035999999999999588 ) ) ;
#16421=CARTESIAN_POINT ( 'NONE',  ( -4.138038291653009905E-15, 8.014718854569428785, 4.118099735505521330 ) ) ;
#16460=AXIS2_PLACEMENT_3D ( 'NONE', #2947, #22420, #17443 ) ;
#16514=VERTEX_POINT ( 'NONE', #17042 ) ;
#16540=ORIENTED_EDGE ( 'NONE', *, *, #15877, .F. ) ;
#16544=DIRECTION ( 'NONE',  ( 0.000000000000000000, 0.000000000000000000, -1.000000000000000000 ) ) ;
#16596=PLANE ( 'NONE',  #13655 ) ;
#16613=ADVANCED_FACE ( 'NONE', ( #20608 ), #25166, .T. ) ;
#16693=CARTESIAN_POINT ( 'NONE',  ( 7.500000000000000000, 0.000000000000000000, 0.000000000000000000 ) ) ;
#16694=CARTESIAN_POINT ( 'NONE',  ( 0.8038475772933646457, 5.196152422706634688, -9.000000000000001776 ) ) ;
#16732=DIRECTION ( 'NONE',  ( -1.000000000000000000, -0.000000000000000000, -0.000000000000000000 ) ) ;
#16734=ORIENTED_EDGE ( 'NONE', *, *, #17743, .F. ) ;
#16925=FACE_OUTER_BOUND ( 'NONE', #1112, .T. ) ;
#16958=LINE ( 'NONE', #5425, #28579 ) ;
#16962=CARTESIAN_POINT ( 'NONE',  ( 6.899999999999999467, 5.196152422706634688, -9.000000000000001776 ) ) ;
#17017=CARTESIAN_POINT ( 'NONE',  ( 5.412540532954977194E-16, -0.8794428697894915992, -9.000000000000001776 ) ) ;
#17020=CARTESIAN_POINT ( 'NONE',  ( 0.3570196857253488676, 6.047589086024998117, -7.525268439705683043 ) ) ;
#17042=CARTESIAN_POINT ( 'NONE',  ( 8.099999999999999645, 0.000000000000000000, 6.000000000000001776 ) ) ;
#17055=DIRECTION ( 'NONE',  ( 1.000000000000000000, 0.000000000000000000, 0.000000000000000000 ) ) ;
#17112=DIRECTION ( 'NONE',  ( 0.000000000000000000, 0.5000000000000015543, -0.8660254037844378194 ) ) ;
#17115=ORIENTED_EDGE ( 'NONE', *, *, #11545, .F. ) ;
#17173=CARTESIAN_POINT ( 'NONE',  ( 0.5590800469813631546, 5.620102221249823060, -8.265697409064610923 ) ) ;
#17174=ORIENTED_EDGE ( 'NONE', *, *, #6716, .T. ) ;
#17228=PLANE ( 'NONE',  #8481 ) ;
#17298=DIRECTION ( 'NONE',  ( 0.000000000000000000, 0.000000000000000000, -1.000000000000000000 ) ) ;
#17311=ORIENTED_EDGE ( 'NONE', *, *, #10589, .T. ) ;
#17325=ORIENTED_EDGE ( 'NONE', *, *, #15877, .T. ) ;
#17443=DIRECTION ( 'NONE',  ( 0.000000000000000000, 0.000000000000000000, -1.000000000000000000 ) ) ;
#17447=CIRCLE ( 'NONE', #12469, 6.600000000000001421 ) ;
#17461=EDGE_CURVE ( 'NONE', #26638, #7128, #7999, .T. ) ;
#17617=ORIENTED_EDGE ( 'NONE', *, *, #5134, .F. ) ;
#17636=PRODUCT_DEFINITION_CONTEXT ( 'detailed design', #2417, 'design' ) ;
#17657=FACE_OUTER_BOUND ( 'NONE', #17725, .T. ) ;
#17678=AXIS2_PLACEMENT_3D ( 'NONE', #5041, #15004, #21556 ) ;
#17725=EDGE_LOOP ( 'NONE', ( #22952, #18753 ) ) ;
#17743=EDGE_CURVE ( 'NONE', #281, #10722, #20722, .T. ) ;
#17803=AXIS2_PLACEMENT_3D ( 'NONE', #21393, #10017, #12047 ) ;
#17810=VECTOR ( 'NONE', #20880, 1000.000000000000114 ) ;
#17828=CIRCLE ( 'NONE', #13353, 6.000000000000001776 ) ;
#17844=DIRECTION ( 'NONE',  ( 0.000000000000000000, 0.000000000000000000, -1.000000000000000000 ) ) ;
#17895=CARTESIAN_POINT ( 'NONE',  ( 0.000000000000000000, 7.794228634059944483, -4.500000000000004441 ) ) ;
#17897=AXIS2_PLACEMENT_3D ( 'NONE', #8547, #30203, #4006 ) ;
#18014=ORIENTED_EDGE ( 'NONE', *, *, #4558, .T. ) ;
#18106=B_SPLINE_CURVE_WITH_KNOTS ( 'NONE', 3,
 ( #21764, #2749, #12576, #10533, #27070, #15191, #22224, #12259 ),
 .UNSPECIFIED., .F., .F.,
 ( 4, 2, 2, 4 ),
 ( 0.005257893453559912313, 0.006567392922673243386, 0.007876892391786575326, 0.01049589133001323574 ),
 .UNSPECIFIED. ) ;
#18140=DIRECTION ( 'NONE',  ( -1.000000000000000000, -0.000000000000000000, -0.000000000000000000 ) ) ;
#18184=DIRECTION ( 'NONE',  ( -1.000000000000000000, -0.000000000000000000, -0.000000000000000000 ) ) ;
#18194=CARTESIAN_POINT ( 'NONE',  ( 0.07661102881318006264, 8.673996836102553232, -2.976196775178694853 ) ) ;
#18288=ORIENTED_EDGE ( 'NONE', *, *, #1029, .T. ) ;
#18309=CARTESIAN_POINT ( 'NONE',  ( 6.511989298491061007E-15, -8.236864015571844888, 3.733333029993807006 ) ) ;
#18312=CARTESIAN_POINT ( 'NONE',  ( 0.000000000000000000, 7.794228634059939154, 4.500000000000010658 ) ) ;
#18354=CARTESIAN_POINT ( 'NONE',  ( 0.8038475772933696417, 10.39230484541327471, -1.336447385876663028E-16 ) ) ;
#18376=ORIENTED_EDGE ( 'NONE', *, *, #17461, .T. ) ;
#18383=ORIENTED_EDGE ( 'NONE', *, *, #24612, .F. ) ;
#18399=EDGE_CURVE ( 'NONE', #29153, #11604, #12456, .T. ) ;
#18479=AXIS2_PLACEMENT_3D ( 'NONE', #22261, #7771, #5274 ) ;
#18490=ORIENTED_EDGE ( 'NONE', *, *, #2170, .T. ) ;
#18512=VERTEX_POINT ( 'NONE', #22156 ) ;
#18536=VERTEX_POINT ( 'NONE', #12662 ) ;
#18555=CARTESIAN_POINT ( 'NONE',  ( 6.900000000000000355, 0.000000000000000000, 0.000000000000000000 ) ) ;
#18560=EDGE_LOOP ( 'NONE', ( #14700, #17174, #29840 ) ) ;
#18586=ORIENTED_EDGE ( 'NONE', *, *, #28057, .T. ) ;
#18594=VECTOR ( 'NONE', #11273, 1000.000000000000000 ) ;
#18596=DIRECTION ( 'NONE',  ( 1.000000000000000000, 0.000000000000000000, -0.000000000000000000 ) ) ;
#18607=EDGE_LOOP ( 'NONE', ( #29022, #1817, #4132 ) ) ;
#18614=CARTESIAN_POINT ( 'NONE',  ( 0.07661102881318986035, -8.673996836102570995, 2.976196775178701515 ) ) ;
#18730=ORIENTED_EDGE ( 'NONE', *, *, #28232, .T. ) ;
#18736=EDGE_LOOP ( 'NONE', ( #9505, #23098, #1898 ) ) ;
#18744=CARTESIAN_POINT ( 'NONE',  ( 0.3552109633508242492, -3.484997970623515684, 9.000000000000003553 ) ) ;
#18753=ORIENTED_EDGE ( 'NONE', *, *, #13534, .T. ) ;
#18838=ADVANCED_FACE ( 'NONE', ( #25512 ), #25185, .T. ) ;
#18860=DIRECTION ( 'NONE',  ( -1.000000000000000000, -0.000000000000000000, -0.000000000000000000 ) ) ;
#18898=VERTEX_POINT ( 'NONE', #69 ) ;
#18929=VERTEX_POINT ( 'NONE', #21726 ) ;
#19019=CARTESIAN_POINT ( 'NONE',  ( 8.099999999999999645, 7.347880794884121708E-16, -6.000000000000001776 ) ) ;
#19037=CARTESIAN_POINT ( 'NONE',  ( 0.09318607064769421355, 1.767053008364807942, -9.000000000000003553 ) ) ;
#19065=ORIENTED_EDGE ( 'NONE', *, *, #14946, .T. ) ;
#19068=EDGE_CURVE ( 'NONE', #26638, #7923, #27767, .T. ) ;
#19095=CARTESIAN_POINT ( 'NONE',  ( 0.8038475772933700858, -5.196152422706651564, 9.000000000000001776 ) ) ;
#19121=FACE_OUTER_BOUND ( 'NONE', #18736, .T. ) ;
#19144=ADVANCED_FACE ( 'NONE', ( #1068 ), #3720, .F. ) ;
#19175=ORIENTED_EDGE ( 'NONE', *, *, #21369, .F. ) ;
#19184=ORIENTED_EDGE ( 'NONE', *, *, #20210, .F. ) ;
#19216=FACE_OUTER_BOUND ( 'NONE', #3898, .T. ) ;
#19282=FACE_OUTER_BOUND ( 'NONE', #29754, .T. ) ;
#19368=CARTESIAN_POINT ( 'NONE',  ( 0.1469846612282507681, 6.696526368584472699, -6.401276095386996268 ) ) ;
#19386=AXIS2_PLACEMENT_3D ( 'NONE', #16269, #25791, #25491 ) ;
#19403=ORIENTED_EDGE ( 'NONE', *, *, #5134, .T. ) ;
#19419=DIRECTION ( 'NONE',  ( -1.000000000000000000, 0.000000000000000000, -0.000000000000000000 ) ) ;
#19530=CARTESIAN_POINT ( 'NONE',  ( 6.899999999999999467, -5.196152422706639129, -9.000000000000000000 ) ) ;
#19598=EDGE_LOOP ( 'NONE', ( #3094, #5325, #11181, #8756, #30311, #5515 ) ) ;
#19695=CARTESIAN_POINT ( 'NONE',  ( 0.000000000000000000, 0.000000000000000000, 0.000000000000000000 ) ) ;
#19722=PRODUCT_CONTEXT ( 'NONE', #10574, 'mechanical' ) ;
#19763=DIRECTION ( 'NONE',  ( -1.000000000000000000, -0.000000000000000000, -0.000000000000000000 ) ) ;
#19820=LINE ( 'NONE', #7986, #29525 ) ;
#19928=CARTESIAN_POINT ( 'NONE',  ( -4.225000340904450091E-15, 7.351593252548064505, 5.266666970006215642 ) ) ;
#19989=CARTESIAN_POINT ( 'NONE',  ( 0.09318607064769342252, 1.767053008364804167, 9.000000000000000000 ) ) ;
#20054=CIRCLE ( 'NONE', #24021, 9.000000000000000000 ) ;
#20155=EDGE_LOOP ( 'NONE', ( #11927, #12013, #24527, #705, #28221, #2330 ) ) ;
#20158=DIRECTION ( 'NONE',  ( 0.000000000000000000, 0.000000000000000000, -1.000000000000000000 ) ) ;
#20193=DIRECTION ( 'NONE',  ( -0.000000000000000000, 0.5000000000000005551, 0.8660254037844382635 ) ) ;
#20199=CARTESIAN_POINT ( 'NONE',  ( 0.000000000000000000, 4.336808689942017736E-15, -17.99999999999998224 ) ) ;
#20210=EDGE_CURVE ( 'NONE', #15949, #18536, #30368, .T. ) ;
#20224=ORIENTED_EDGE ( 'NONE', *, *, #30007, .T. ) ;
#20260=DIRECTION ( 'NONE',  ( 1.000000000000000000, 0.000000000000000000, -0.000000000000000000 ) ) ;
#20322=CARTESIAN_POINT ( 'NONE',  ( 0.000000000000000000, 0.000000000000000000, 0.000000000000000000 ) ) ;
#20333=AXIS2_PLACEMENT_3D ( 'NONE', #11864, #28702, #2 ) ;
#20376=VECTOR ( 'NONE', #11171, 1000.000000000000000 ) ;
#20463=ADVANCED_FACE ( 'NONE', ( #19121 ), #1351, .T. ) ;
#20514=FACE_OUTER_BOUND ( 'NONE', #21663, .T. ) ;
#20529=( NAMED_UNIT ( * ) PLANE_ANGLE_UNIT ( ) SI_UNIT ( $, .RADIAN. ) );
#20542=ORIENTED_EDGE ( 'NONE', *, *, #17461, .F. ) ;
#20593=CARTESIAN_POINT ( 'NONE',  ( 0.000000000000000000, 0.000000000000000000, 0.000000000000000000 ) ) ;
#20608=FACE_OUTER_BOUND ( 'NONE', #13300, .T. ) ;
#20722=CIRCLE ( 'NONE', #7293, 0.5999999999999998668 ) ;
#20742=FACE_OUTER_BOUND ( 'NONE', #30179, .T. ) ;
#20759=FACE_OUTER_BOUND ( 'NONE', #11251, .T. ) ;
#20794=DIRECTION ( 'NONE',  ( -1.000000000000000000, -0.000000000000000000, -0.000000000000000000 ) ) ;
#20835=AXIS2_PLACEMENT_3D ( 'NONE', #1143, #12703, #17844 ) ;
#20875=ORIENTED_EDGE ( 'NONE', *, *, #9017, .T. ) ;
#20880=DIRECTION ( 'NONE',  ( -0.000000000000000000, 0.5000000000000005551, 0.8660254037844382635 ) ) ;
#20987=CARTESIAN_POINT ( 'NONE',  ( 6.899999999999999467, -5.196152422706639129, -9.000000000000000000 ) ) ;
#21013=EDGE_CURVE ( 'NONE', #11068, #12149, #22781, .T. ) ;
#21014=DIRECTION ( 'NONE',  ( 1.000000000000000000, 0.000000000000000000, 0.000000000000000000 ) ) ;
#21059=EDGE_CURVE ( 'NONE', #16129, #27888, #23207, .T. ) ;
#21155=CARTESIAN_POINT ( 'NONE',  ( 8.099999999999999645, 8.082668874372532992E-16, 6.600000000000001421 ) ) ;
#21181=ORIENTED_EDGE ( 'NONE', *, *, #293, .F. ) ;
#21213=CARTESIAN_POINT ( 'NONE',  ( 0.07568653364412146478, -1.751902528157389893, 9.000000000000000000 ) ) ;
#21272=LINE ( 'NONE', #25519, #20376 ) ;
#21291=CONICAL_SURFACE ( 'NONE', #24287, 9.000000000000000000, 1.047197551196600296 ) ;
#21369=EDGE_CURVE ( 'NONE', #7440, #2660, #25388, .T. ) ;
#21391=( GEOMETRIC_REPRESENTATION_CONTEXT ( 3 ) GLOBAL_UNCERTAINTY_ASSIGNED_CONTEXT ( ( #25469 ) ) GLOBAL_UNIT_ASSIGNED_CONTEXT ( ( #30684, #26329, #25871 ) ) REPRESENTATION_CONTEXT ( 'NONE', 'WORKASPACE' ) );
#21393=CARTESIAN_POINT ( 'NONE',  ( 0.000000000000000000, 0.000000000000000000, 0.000000000000000000 ) ) ;
#21408=ORIENTED_EDGE ( 'NONE', *, *, #28232, .F. ) ;
#21430=DIRECTION ( 'NONE',  ( 0.000000000000000000, -0.5000000000000005551, -0.8660254037844382635 ) ) ;
#21437=LINE ( 'NONE', #79, #15378 ) ;
#21474=ORIENTED_EDGE ( 'NONE', *, *, #6728, .T. ) ;
#21556=DIRECTION ( 'NONE',  ( 0.000000000000000000, -1.000000000000000000, 1.669238443041286689E-16 ) ) ;
#21585=AXIS2_PLACEMENT_3D ( 'NONE', #10792, #13460, #8304 ) ;
#21590=CARTESIAN_POINT ( 'NONE',  ( 1.010086789600752760E-15, 0.4400770685579618036, 9.000000000000001776 ) ) ;
#21640=DIRECTION ( 'NONE',  ( 0.000000000000000000, 1.000000000000000000, -1.669238443041286689E-16 ) ) ;
#21663=EDGE_LOOP ( 'NONE', ( #24034, #19403, #9132, #23328 ) ) ;
#21694=CARTESIAN_POINT ( 'NONE',  ( 7.500000000000000000, 5.196152422706624030, 9.000000000000001776 ) ) ;
#21726=CARTESIAN_POINT ( 'NONE',  ( 7.500000000000000000, 0.000000000000000000, 9.000000000000000000 ) ) ;
#21738=CARTESIAN_POINT ( 'NONE',  ( 0.5612050131688001153, 4.355613924421556149, 9.000000000000001776 ) ) ;
#21743=VECTOR ( 'NONE', #9696, 1000.000000000000000 ) ;
#21764=CARTESIAN_POINT ( 'NONE',  ( 0.000000000000000000, -7.794228634059943595, 4.500000000000005329 ) ) ;
#21831=CARTESIAN_POINT ( 'NONE',  ( 0.01885174614965991896, 0.8831628876357848767, -9.000000000000003553 ) ) ;
#21923=PRODUCT_DEFINITION ( 'UNKNOWN', '', #14376, #17636 ) ;
#21953=DIRECTION ( 'NONE',  ( 0.000000000000000000, 0.000000000000000000, -1.000000000000000000 ) ) ;
#22002=DIRECTION ( 'NONE',  ( 0.000000000000000000, -1.000000000000000000, 0.000000000000000000 ) ) ;
#22141=DIRECTION ( 'NONE',  ( 1.000000000000000000, 0.000000000000000000, -0.000000000000000000 ) ) ;
#22156=CARTESIAN_POINT ( 'NONE',  ( 6.899999999999999467, 5.196152422706634688, -9.000000000000001776 ) ) ;
#22213=CARTESIAN_POINT ( 'NONE',  ( 0.07661102881317785607, -6.914460432017389024, -6.023803224821256741 ) ) ;
#22224=CARTESIAN_POINT ( 'NONE',  ( 0.5590800469813690388, -5.620102221249836383, 8.265697409064610923 ) ) ;
#22261=CARTESIAN_POINT ( 'NONE',  ( 0.000000000000000000, 0.000000000000000000, 0.000000000000000000 ) ) ;
#22420=DIRECTION ( 'NONE',  ( 1.000000000000000000, 0.000000000000000000, -0.000000000000000000 ) ) ;
#22447=ORIENTED_EDGE ( 'NONE', *, *, #23082, .T. ) ;
#22464=CARTESIAN_POINT ( 'NONE',  ( -2.195509399283147268E-15, 7.573738413550469062, -4.881900264494495545 ) ) ;
#22488=EDGE_CURVE ( 'NONE', #2369, #2413, #1776, .T. ) ;
#22499=PLANE ( 'NONE',  #20835 ) ;
#22535=CARTESIAN_POINT ( 'NONE',  ( 6.899999999999999467, 5.196152422706634688, -9.000000000000001776 ) ) ;
#22781=CIRCLE ( 'NONE', #15818, 9.000000000000000000 ) ;
#22801=DIRECTION ( 'NONE',  ( -1.000000000000000000, -0.000000000000000000, -0.000000000000000000 ) ) ;
#22851=DIRECTION ( 'NONE',  ( 0.000000000000000000, 0.000000000000000000, 1.000000000000000000 ) ) ;
#22935=ORIENTED_EDGE ( 'NONE', *, *, #6049, .F. ) ;
#22952=ORIENTED_EDGE ( 'NONE', *, *, #13636, .T. ) ;
#22998=CARTESIAN_POINT ( 'NONE',  ( 6.900000000000000355, 0.000000000000000000, 0.000000000000000000 ) ) ;
#23014=CARTESIAN_POINT ( 'NONE',  ( 0.000000000000000000, -7.794228634059938265, -4.500000000000013323 ) ) ;
#23065=ORIENTED_EDGE ( 'NONE', *, *, #22488, .T. ) ;
#23082=EDGE_CURVE ( 'NONE', #23209, #15949, #13668, .T. ) ;
#23098=ORIENTED_EDGE ( 'NONE', *, *, #6296, .T. ) ;
#23116=DIRECTION ( 'NONE',  ( -1.000000000000000000, -0.000000000000000000, -0.000000000000000000 ) ) ;
#23144=CONICAL_SURFACE ( 'NONE', #27153, 5.035999999999999588, 0.7853981633974388421 ) ;
#23207=LINE ( 'NONE', #11386, #17810 ) ;
#23209=VERTEX_POINT ( 'NONE', #1250 ) ;
#23217=CARTESIAN_POINT ( 'NONE',  ( 0.3570196857253589706, -9.540868182094921934, -1.474731560294328947 ) ) ;
#23328=ORIENTED_EDGE ( 'NONE', *, *, #5768, .T. ) ;
#23353=AXIS2_PLACEMENT_3D ( 'NONE', #16693, #10244, #7932 ) ;
#23377=MANIFOLD_SOLID_BREP ( 'HeadFillet', #2359 ) ;
#23394=DIRECTION ( 'NONE',  ( 0.000000000000000000, 0.000000000000000000, -1.000000000000000000 ) ) ;
#23558=CARTESIAN_POINT ( 'NONE',  ( 0.8038475772933700858, -5.196152422706651564, 9.000000000000001776 ) ) ;
#23572=LINE ( 'NONE', #2062, #12069 ) ;
#23583=DIRECTION ( 'NONE',  ( 0.000000000000000000, -0.5000000000000015543, 0.8660254037844378194 ) ) ;
#23607=FACE_OUTER_BOUND ( 'NONE', #2014, .T. ) ;
#23624=CARTESIAN_POINT ( 'NONE',  ( 0.000000000000000000, 0.000000000000000000, 0.000000000000000000 ) ) ;
#23631=EDGE_CURVE ( 'NONE', #7923, #26638, #5468, .T. ) ;
#23653=DIRECTION ( 'NONE',  ( -0.000000000000000000, 1.000000000000000000, -1.224646799147353207E-16 ) ) ;
#23714=CARTESIAN_POINT ( 'NONE',  ( 0.07568653364412844531, -1.751902528157471828, -9.000000000000000000 ) ) ;
#23742=DIRECTION ( 'NONE',  ( 0.000000000000000000, 0.000000000000000000, 1.000000000000000000 ) ) ;
#23752=AXIS2_PLACEMENT_3D ( 'NONE', #24940, #20260, #10915 ) ;
#23756=CARTESIAN_POINT ( 'NONE',  ( 0.000000000000000000, 0.000000000000000000, 0.000000000000000000 ) ) ;
#23760=VERTEX_POINT ( 'NONE', #511 ) ;
#23852=EDGE_CURVE ( 'NONE', #10722, #7638, #17447, .T. ) ;
#23856=PRODUCT ( 'hex bolt gradeab_iso_ISO 4014 - M12 x 120 x 30-N', 'hex bolt gradeab_iso_ISO 4014 - M12 x 120 x 30-N', '', ( #19722 ) ) ;
#23962=CARTESIAN_POINT ( 'NONE',  ( 6.899999999999999467, 9.000000000000000000, 0.000000000000000000 ) ) ;
#24004=CARTESIAN_POINT ( 'NONE',  ( 0.000000000000000000, -1.502314598737157848E-15, -9.000000000000001776 ) ) ;
#24021=AXIS2_PLACEMENT_3D ( 'NONE', #82, #25670, #11484 ) ;
#24022=CARTESIAN_POINT ( 'NONE',  ( 0.8038475772933806329, -10.39230484541329247, 6.144194323733775069E-17 ) ) ;
#24034=ORIENTED_EDGE ( 'NONE', *, *, #6342, .F. ) ;
#24221=DIRECTION ( 'NONE',  ( 0.000000000000000000, 0.000000000000000000, -1.000000000000000000 ) ) ;
#24275=DIRECTION ( 'NONE',  ( -1.000000000000000000, -0.000000000000000000, -0.000000000000000000 ) ) ;
#24287=AXIS2_PLACEMENT_3D ( 'NONE', #11640, #4930, #25994 ) ;
#24298=FACE_OUTER_BOUND ( 'NONE', #30604, .T. ) ;
#24371=EDGE_LOOP ( 'NONE', ( #29582, #1531 ) ) ;
#24372=EDGE_LOOP ( 'NONE', ( #7726, #11822, #11307, #13864, #589, #21408 ) ) ;
#24395=CARTESIAN_POINT ( 'NONE',  ( 0.000000000000000000, 7.794228634059939154, 4.500000000000010658 ) ) ;
#24521=CIRCLE ( 'NONE', #1131, 6.000000000000001776 ) ;
#24527=ORIENTED_EDGE ( 'NONE', *, *, #2510, .F. ) ;
#24566=EDGE_CURVE ( 'NONE', #14545, #13653, #29922, .T. ) ;
#24578=ORIENTED_EDGE ( 'NONE', *, *, #21013, .F. ) ;
#24612=EDGE_CURVE ( 'NONE', #14253, #2413, #27936, .T. ) ;
#24614=ADVANCED_FACE ( 'NONE', ( #24298 ), #12465, .T. ) ;
#24635=DIRECTION ( 'NONE',  ( 0.000000000000000000, 0.000000000000000000, -1.000000000000000000 ) ) ;
#24717=VECTOR ( 'NONE', #10632, 1000.000000000000114 ) ;
#24789=VECTOR ( 'NONE', #6509, 1000.000000000000000 ) ;
#24807=EDGE_LOOP ( 'NONE', ( #20542, #12240, #2424, #17617 ) ) ;
#24818=ORIENTED_EDGE ( 'NONE', *, *, #30532, .F. ) ;
#24831=DIRECTION ( 'NONE',  ( 1.000000000000000000, 0.000000000000000000, -0.000000000000000000 ) ) ;
#24841=CARTESIAN_POINT ( 'NONE',  ( 127.5000000000000000, 0.000000000000000000, 0.000000000000000000 ) ) ;
#24940=CARTESIAN_POINT ( 'NONE',  ( 0.000000000000000000, 0.000000000000000000, 0.000000000000000000 ) ) ;
#25057=CARTESIAN_POINT ( 'NONE',  ( 0.8038475772933620922, 5.196152422706624030, 9.000000000000001776 ) ) ;
#25066=CARTESIAN_POINT ( 'NONE',  ( 7.500000000000000000, -5.196152422706650675, 9.000000000000001776 ) ) ;
#25104=B_SPLINE_CURVE_WITH_KNOTS ( 'NONE', 3,
 ( #18312, #16421, #2220, #30764, #27830, #13489, #6459, #11287 ),
 .UNSPECIFIED., .F., .F.,
 ( 4, 2, 2, 4 ),
 ( 0.005257893453559881955, 0.006567392922673221702, 0.007876892391786561448, 0.01049589133001324094 ),
 .UNSPECIFIED. ) ;
#25166=CONICAL_SURFACE ( 'NONE', #3256, 5.035999999999999588, 0.7853981633974388421 ) ;
#25171=ORIENTED_EDGE ( 'NONE', *, *, #13063, .T. ) ;
#25185=CYLINDRICAL_SURFACE ( 'NONE', #360, 6.000000000000001776 ) ;
#25217=CIRCLE ( 'NONE', #7859, 9.000000000000000000 ) ;
#25251=CARTESIAN_POINT ( 'NONE',  ( 6.900000000000000355, -7.794228634059938265, -4.500000000000013323 ) ) ;
#25375=( NAMED_UNIT ( * ) SI_UNIT ( $, .STERADIAN. ) SOLID_ANGLE_UNIT ( ) );
#25388=LINE ( 'NONE', #20987, #24789 ) ;
#25389=ADVANCED_FACE ( 'NONE', ( #5712 ), #3378, .F. ) ;
#25390=EDGE_LOOP ( 'NONE', ( #7371, #27789 ) ) ;
#25450=FACE_OUTER_BOUND ( 'NONE', #9284, .T. ) ;
#25469=UNCERTAINTY_MEASURE_WITH_UNIT (LENGTH_MEASURE( 1.000000000000000082E-05 ), #30684, 'distance_accuracy_value', 'NONE');
#25491=DIRECTION ( 'NONE',  ( 0.000000000000000000, 0.000000000000000000, 1.000000000000000000 ) ) ;
#25498=ADVANCED_FACE ( 'NONE', ( #23607 ), #2250, .T. ) ;
#25512=FACE_OUTER_BOUND ( 'NONE', #14417, .T. ) ;
#25519=CARTESIAN_POINT ( 'NONE',  ( 6.899999999999999467, 5.196152422706624030, 9.000000000000001776 ) ) ;
#25569=ADVANCED_FACE ( 'NONE', ( #20759 ), #10807, .T. ) ;
#25670=DIRECTION ( 'NONE',  ( -1.000000000000000000, -0.000000000000000000, -0.000000000000000000 ) ) ;
#25791=DIRECTION ( 'NONE',  ( -1.000000000000000000, -0.000000000000000000, -0.000000000000000000 ) ) ;
#25871=( NAMED_UNIT ( * ) SI_UNIT ( $, .STERADIAN. ) SOLID_ANGLE_UNIT ( ) );
#25994=DIRECTION ( 'NONE',  ( 0.000000000000000000, 0.000000000000000000, -1.000000000000000000 ) ) ;
#26005=AXIS2_PLACEMENT_3D ( 'NONE', #7206, #5754, #14538 ) ;
#26052=DIRECTION ( 'NONE',  ( 1.000000000000000000, 0.000000000000000000, -0.000000000000000000 ) ) ;
#26076=CYLINDRICAL_SURFACE ( 'NONE', #17803, 9.000000000000000000 ) ;
#26098=PRODUCT_DEFINITION_SHAPE ( 'NONE', 'NONE',  #21923 ) ;
#26110=CARTESIAN_POINT ( 'NONE',  ( 7.500000000000000000, 5.196152422706634688, -9.000000000000001776 ) ) ;
#26161=VERTEX_POINT ( 'NONE', #14909 ) ;
#26217=CARTESIAN_POINT ( 'NONE',  ( 0.5595136366802240246, -4.349754824395735575, 9.000000000000001776 ) ) ;
#26234=AXIS2_PLACEMENT_3D ( 'NONE', #6453, #23116, #173 ) ;
#26240=PLANE ( 'NONE',  #10095 ) ;
#26242=PLANE ( 'NONE',  #17678 ) ;
#26255=CARTESIAN_POINT ( 'NONE',  ( 6.899999999999999467, -5.196152422706651564, 9.000000000000001776 ) ) ;
#26273=CARTESIAN_POINT ( 'NONE',  ( 0.8038475772933620922, 5.196152422706624030, 9.000000000000001776 ) ) ;
#26314=VERTEX_POINT ( 'NONE', #26255 ) ;
#26329=( NAMED_UNIT ( * ) PLANE_ANGLE_UNIT ( ) SI_UNIT ( $, .RADIAN. ) );
#26343=ORIENTED_EDGE ( 'NONE', *, *, #21369, .T. ) ;
#26367=EDGE_CURVE ( 'NONE', #13653, #15949, #28441, .T. ) ;
#26443=CARTESIAN_POINT ( 'NONE',  ( 7.500000000000000000, 5.196152422706624030, 9.000000000000001776 ) ) ;
#26546=CARTESIAN_POINT ( 'NONE',  ( 126.5359999999999872, 0.000000000000000000, 6.000000000000001776 ) ) ;
#26600=VERTEX_POINT ( 'NONE', #24022 ) ;
#26636=DIRECTION ( 'NONE',  ( 0.000000000000000000, 1.224646799147354933E-16, 1.000000000000000000 ) ) ;
#26638=VERTEX_POINT ( 'NONE', #16403 ) ;
#26681=UNCERTAINTY_MEASURE_WITH_UNIT (LENGTH_MEASURE( 1.000000000000000082E-05 ), #27417, 'distance_accuracy_value', 'NONE');
#26693=CARTESIAN_POINT ( 'NONE',  ( 0.8038475772933646457, 5.196152422706634688, -9.000000000000001776 ) ) ;
#26718=EDGE_CURVE ( 'NONE', #10711, #16514, #19820, .T. ) ;
#26799=EDGE_CURVE ( 'NONE', #12149, #26314, #323, .T. ) ;
#26862=LINE ( 'NONE', #1110, #8849 ) ;
#26869=ORIENTED_EDGE ( 'NONE', *, *, #293, .T. ) ;
#26885=EDGE_LOOP ( 'NONE', ( #15448, #967, #1328, #24818 ) ) ;
#26894=MECHANICAL_DESIGN_GEOMETRIC_PRESENTATION_REPRESENTATION('',(#27897),#21391);
#26921=CARTESIAN_POINT ( 'NONE',  ( 6.900000000000000355, 7.794228634059944483, -4.500000000000004441 ) ) ;
#26965=B_SPLINE_CURVE_WITH_KNOTS ( 'NONE', 3,
 ( #15287, #22464, #29349, #9854, #19368, #17020, #17173, #26693 ),
 .UNSPECIFIED., .F., .F.,
 ( 4, 2, 2, 4 ),
 ( 0.005257893453559900170, 0.006567392922673233845, 0.007876892391786568387, 0.01049589133001323400 ),
 .UNSPECIFIED. ) ;
#26984=AXIS2_PLACEMENT_3D ( 'NONE', #12999, #30290, #20158 ) ;
#27001=ORIENTED_EDGE ( 'NONE', *, *, #9609, .T. ) ;
#27038=VECTOR ( 'NONE', #28007, 1000.000000000000114 ) ;
#27070=CARTESIAN_POINT ( 'NONE',  ( 0.1469846612282592335, -6.696526368584486022, 6.401276095386999820 ) ) ;
#27116=VECTOR ( 'NONE', #21640, 1000.000000000000000 ) ;
#27153=AXIS2_PLACEMENT_3D ( 'NONE', #5342, #14853, #14552 ) ;
#27280=VECTOR ( 'NONE', #28076, 1000.000000000000000 ) ;
#27400=DIRECTION ( 'NONE',  ( 1.000000000000000000, 0.000000000000000000, -0.000000000000000000 ) ) ;
#27417=( LENGTH_UNIT ( ) NAMED_UNIT ( * ) SI_UNIT ( .MILLI., .METRE. ) );
#27557=CARTESIAN_POINT ( 'NONE',  ( 0.000000000000000000, 7.347880794884121708E-16, -6.000000000000001776 ) ) ;
#27568=ORIENTED_EDGE ( 'NONE', *, *, #9784, .F. ) ;
#27577=VECTOR ( 'NONE', #20794, 1000.000000000000000 ) ;
#27664=CARTESIAN_POINT ( 'NONE',  ( 0.8038475772933806329, -10.39230484541329247, 6.144194323733775069E-17 ) ) ;
#27673=EDGE_CURVE ( 'NONE', #26314, #11068, #16251, .T. ) ;
#27696=DIRECTION ( 'NONE',  ( 0.000000000000000000, 0.000000000000000000, 1.000000000000000000 ) ) ;
#27701=CARTESIAN_POINT ( 'NONE',  ( 7.500000000000000000, -10.39230484541329247, 8.776157072412030708E-17 ) ) ;
#27767=CIRCLE ( 'NONE', #15321, 5.035999999999999588 ) ;
#27789=ORIENTED_EDGE ( 'NONE', *, *, #19068, .F. ) ;
#27798=VECTOR ( 'NONE', #8973, 1000.000000000000000 ) ;
#27812=DIRECTION ( 'NONE',  ( 0.000000000000000000, 0.000000000000000000, 1.000000000000000000 ) ) ;
#27830=CARTESIAN_POINT ( 'NONE',  ( 0.1469846612282506015, 8.891930899535427812, 2.598723904613014835 ) ) ;
#27831=LINE ( 'NONE', #3808, #10118 ) ;
#27839=LINE ( 'NONE', #1779, #27577 ) ;
#27857=DIRECTION ( 'NONE',  ( -1.000000000000000000, -0.000000000000000000, -0.000000000000000000 ) ) ;
#27888=VERTEX_POINT ( 'NONE', #2210 ) ;
#27897=STYLED_ITEM('',(#30907),#23377);
#27936=CIRCLE ( 'NONE', #18479, 9.000000000000000000 ) ;
#27962=CARTESIAN_POINT ( 'NONE',  ( 127.5000000000000000, 0.000000000000000000, 0.000000000000000000 ) ) ;
#27966=DIRECTION ( 'NONE',  ( -1.000000000000000000, -0.000000000000000000, -0.000000000000000000 ) ) ;
#27967=CARTESIAN_POINT ( 'NONE',  ( 6.899999999999999467, -10.39230484541329247, 8.776157072412030708E-17 ) ) ;
#27973=CARTESIAN_POINT ( 'NONE',  ( 0.3563104543936492230, -9.539178283403872527, 1.477658550686874017 ) ) ;
#28007=DIRECTION ( 'NONE',  ( -0.7071067811865541231, 0.000000000000000000, 0.7071067811865408004 ) ) ;
#28057=EDGE_CURVE ( 'NONE', #4214, #18898, #26862, .T. ) ;
#28076=DIRECTION ( 'NONE',  ( 0.000000000000000000, -0.5000000000000006661, -0.8660254037844382635 ) ) ;
#28221=ORIENTED_EDGE ( 'NONE', *, *, #4558, .F. ) ;
#28232=EDGE_CURVE ( 'NONE', #11068, #26161, #2020, .T. ) ;
#28402=CARTESIAN_POINT ( 'NONE',  ( 0.3593302862868688052, 3.504574740656565712, -9.000000000000003553 ) ) ;
#28441=CIRCLE ( 'NONE', #8032, 9.000000000000000000 ) ;
#28465=FACE_OUTER_BOUND ( 'NONE', #15159, .T. ) ;
#28514=DIRECTION ( 'NONE',  ( 0.000000000000000000, 0.000000000000000000, 1.000000000000000000 ) ) ;
#28530=CARTESIAN_POINT ( 'NONE',  ( 3.863105514190048694E-15, -8.014718854569434114, -4.118099735505531100 ) ) ;
#28579=VECTOR ( 'NONE', #17112, 1000.000000000000000 ) ;
#28681=CIRCLE ( 'NONE', #1785, 9.000000000000000000 ) ;
#28702=DIRECTION ( 'NONE',  ( -1.000000000000000000, -0.000000000000000000, 0.000000000000000000 ) ) ;
#28731=CARTESIAN_POINT ( 'NONE',  ( 7.500000000000000000, 0.000000000000000000, -6.600000000000001421 ) ) ;
#28745=CARTESIAN_POINT ( 'NONE',  ( 7.500000000000000000, -5.196152422706639129, -9.000000000000000000 ) ) ;
#28789=AXIS2_PLACEMENT_3D ( 'NONE', #7592, #14607, #2603 ) ;
#28808=LINE ( 'NONE', #5253, #30697 ) ;
#28818=LINE ( 'NONE', #268, #2621 ) ;
#28819=ADVANCED_FACE ( 'NONE', ( #19282 ), #7131, .T. ) ;
#28826=ORIENTED_EDGE ( 'NONE', *, *, #14035, .T. ) ;
#28922=FACE_OUTER_BOUND ( 'NONE', #10072, .T. ) ;
#28931=CARTESIAN_POINT ( 'NONE',  ( 0.3593302862868671399, 3.504574740656557275, 9.000000000000003553 ) ) ;
#28994=CARTESIAN_POINT ( 'NONE',  ( 6.900000000000000355, -1.502314598737158242E-15, -9.000000000000001776 ) ) ;
#29022=ORIENTED_EDGE ( 'NONE', *, *, #26799, .T. ) ;
#29125=B_SPLINE_CURVE_WITH_KNOTS ( 'NONE', 3,
 ( #3658, #15811, #3345, #22213, #15345, #1481 ),
 .UNSPECIFIED., .F., .F.,
 ( 4, 2, 4 ),
 ( 2.380730970505090229E-07, 0.002629065763328460210, 0.005257893453559869812 ),
 .UNSPECIFIED. ) ;
#29152=CARTESIAN_POINT ( 'NONE',  ( 8.099999999999999645, 0.000000000000000000, -6.600000000000001421 ) ) ;
#29153=VERTEX_POINT ( 'NONE', #19095 ) ;
#29219=ADVANCED_FACE ( 'NONE', ( #28922 ), #29308, .T. ) ;
#29250=ADVANCED_FACE ( 'NONE', ( #10818 ), #22499, .T. ) ;
#29308=CONICAL_SURFACE ( 'NONE', #1444, 9.000000000000000000, 1.047197551196600296 ) ;
#29349=CARTESIAN_POINT ( 'NONE',  ( 0.01899995639453812973, 7.352259170992722304, -5.265513565426382492 ) ) ;
#29442=CARTESIAN_POINT ( 'NONE',  ( 0.000000000000000000, 7.794228634059939154, 4.500000000000010658 ) ) ;
#29478=CARTESIAN_POINT ( 'NONE',  ( 7.500000000000000000, 1.102182119232617714E-15, -9.000000000000000000 ) ) ;
#29522=DIRECTION ( 'NONE',  ( -1.000000000000000000, -0.000000000000000000, 0.000000000000000000 ) ) ;
#29525=VECTOR ( 'NONE', #12186, 1000.000000000000000 ) ;
#29582=ORIENTED_EDGE ( 'NONE', *, *, #23852, .T. ) ;
#29718=VECTOR ( 'NONE', #19763, 1000.000000000000000 ) ;
#29731=CARTESIAN_POINT ( 'NONE',  ( 127.5000000000000000, 0.000000000000000000, 5.035999999999999588 ) ) ;
#29754=EDGE_LOOP ( 'NONE', ( #11955, #99, #4553 ) ) ;
#29788=EDGE_LOOP ( 'NONE', ( #20875, #15069, #26869 ) ) ;
#29840=ORIENTED_EDGE ( 'NONE', *, *, #6473, .T. ) ;
#29902=DIRECTION ( 'NONE',  ( -1.000000000000000000, -0.000000000000000000, -0.000000000000000000 ) ) ;
#29922=CIRCLE ( 'NONE', #16460, 9.000000000000000000 ) ;
#29938=ORIENTED_EDGE ( 'NONE', *, *, #7514, .T. ) ;
#29966=ADVANCED_FACE ( 'NONE', ( #2121 ), #21291, .T. ) ;
#29998=CARTESIAN_POINT ( 'NONE',  ( 6.900000000000000355, 0.000000000000000000, 0.000000000000000000 ) ) ;
#30007=EDGE_CURVE ( 'NONE', #14545, #29153, #18106, .T. ) ;
#30083=ORIENTED_EDGE ( 'NONE', *, *, #2026, .T. ) ;
#30097=AXIS2_PLACEMENT_3D ( 'NONE', #21155, #23653, #26636 ) ;
#30118=DIRECTION ( 'NONE',  ( 1.000000000000000000, 0.000000000000000000, 0.000000000000000000 ) ) ;
#30179=EDGE_LOOP ( 'NONE', ( #18730, #2856, #21474 ) ) ;
#30203=DIRECTION ( 'NONE',  ( 1.000000000000000000, 0.000000000000000000, -0.000000000000000000 ) ) ;
#30275=CARTESIAN_POINT ( 'NONE',  ( 6.899999999999999467, 9.000000000000000000, 0.000000000000000000 ) ) ;
#30290=DIRECTION ( 'NONE',  ( 1.000000000000000000, 0.000000000000000000, 0.000000000000000000 ) ) ;
#30311=ORIENTED_EDGE ( 'NONE', *, *, #10108, .F. ) ;
#30334=CARTESIAN_POINT ( 'NONE',  ( 6.899999999999999467, 5.196152422706634688, -9.000000000000001776 ) ) ;
#30335=ORIENTED_EDGE ( 'NONE', *, *, #26718, .F. ) ;
#30349=CARTESIAN_POINT ( 'NONE',  ( -2.107417972768699244E-15, 8.236864015571832454, -3.733333029993799013 ) ) ;
#30358=SHAPE_REPRESENTATION_RELATIONSHIP ( 'NONE' , 'NONE' ,  #10307, #2065 ) ;
#30368=B_SPLINE_CURVE_WITH_KNOTS ( 'NONE', 3,
 ( #2673, #17017, #23714, #24, #12188, #4857 ),
 .UNSPECIFIED., .F., .F.,
 ( 4, 2, 4 ),
 ( 0.03045342003272953624, 0.03308352805739835090, 0.03571363608206717249 ),
 .UNSPECIFIED. ) ;
#30382=AXIS2_PLACEMENT_3D ( 'NONE', #4426, #16732, #23742 ) ;
#30454=CARTESIAN_POINT ( 'NONE',  ( 0.000000000000000000, -7.794228634059943595, 4.500000000000005329 ) ) ;
#30473=LINE ( 'NONE', #30334, #27798 ) ;
#30532=EDGE_CURVE ( 'NONE', #7638, #10722, #2402, .T. ) ;
#30537=DIRECTION ( 'NONE',  ( 1.000000000000000000, 0.000000000000000000, -0.000000000000000000 ) ) ;
#30541=ORIENTED_EDGE ( 'NONE', *, *, #10348, .T. ) ;
#30553=CONICAL_SURFACE ( 'NONE', #21585, 9.000000000000000000, 1.047197551196600296 ) ;
#30604=EDGE_LOOP ( 'NONE', ( #26343, #17325, #17311 ) ) ;
#30610=ORIENTED_EDGE ( 'NONE', *, *, #13063, .F. ) ;
#30616=CARTESIAN_POINT ( 'NONE',  ( 0.000000000000000000, 0.000000000000000000, 9.000000000000000000 ) ) ;
#30684=( LENGTH_UNIT ( ) NAMED_UNIT ( * ) SI_UNIT ( .MILLI., .METRE. ) );
#30697=VECTOR ( 'NONE', #14752, 1000.000000000000000 ) ;
#30743=CARTESIAN_POINT ( 'NONE',  ( 9.994988777600744001E-16, -0.8794428697894486335, 9.000000000000001776 ) ) ;
#30752=ADVANCED_FACE ( 'NONE', ( #14298 ), #14841, .F. ) ;
#30764=CARTESIAN_POINT ( 'NONE',  ( 0.09252763182292053634, 8.674330214978047238, 2.975619346028167911 ) ) ;
#30776=ORIENTED_EDGE ( 'NONE', *, *, #9609, .F. ) ;
#30842=VECTOR ( 'NONE', #16364, 1000.000000000000000 ) ;
#30858=CARTESIAN_POINT ( 'NONE',  ( 0.000000000000000000, -7.794228634059943595, 4.500000000000005329 ) ) ;
#30901=COLOUR_RGB('Black',0.12,0.14,0.17);
#30902=FILL_AREA_STYLE_COLOUR('',#30901);
#30903=FILL_AREA_STYLE('',(#30902));
#30904=SURFACE_STYLE_FILL_AREA(#30903);
#30905=SURFACE_SIDE_STYLE('',(#30904));
#30906=SURFACE_STYLE_USAGE(.BOTH.,#30905);
#30907=PRESENTATION_STYLE_ASSIGNMENT((#30906));
ENDSEC;
END-ISO-10303-21;
